ISO-10303-21;
HEADER;
/* Generated by software containing ST-Developer
 * from STEP Tools, Inc. (www.steptools.com) 
 */

FILE_DESCRIPTION(
/* description */ ('PAT-091'),
/* implementation_level */ '2;1');

FILE_NAME(
/* name */ 'Screw bearing cap.step',
/* time_stamp */ '2026-10-27T15:34:44-07:00',
/* author */ (''),
/* organization */ (''),
/* preprocessor_version */ 'ST-DEVELOPER v20.2',
/* originating_system */ 'Autodesk Translation Framework v15.17.0.0',
/* authorisation */ '');

FILE_SCHEMA (('AUTOMOTIVE_DESIGN { 1 0 10303 214 3 1 1 }'));
ENDSEC;

DATA;
#10=MECHANICAL_DESIGN_GEOMETRIC_PRESENTATION_REPRESENTATION('',(#975),#25100);
#755=SHAPE_REPRESENTATION_RELATIONSHIP('SRR','None',#25516,#865);
#865=ADVANCED_BREP_SHAPE_REPRESENTATION('',(#1099),#24986);
#975=STYLED_ITEM('',(#26198),#1099);
#1099=MANIFOLD_SOLID_BREP('Body1',#13252);
#1255=FACE_BOUND('',#2975,.T.);
#1256=FACE_BOUND('',#2979,.T.);
#1257=FACE_BOUND('',#2980,.T.);
#1258=FACE_BOUND('',#2981,.T.);
#1259=FACE_BOUND('',#2982,.T.);
#1260=FACE_BOUND('',#2983,.T.);
#1261=FACE_BOUND('',#2985,.T.);
#1262=FACE_BOUND('',#2986,.T.);
#1263=FACE_BOUND('',#2987,.T.);
#1264=FACE_BOUND('',#2988,.T.);
#1265=FACE_BOUND('',#2989,.T.);
#1668=PLANE('',#14695);
#1669=PLANE('',#14702);
#1670=PLANE('',#14703);
#2111=FACE_OUTER_BOUND('',#2969,.T.);
#2112=FACE_OUTER_BOUND('',#2970,.T.);
#2113=FACE_OUTER_BOUND('',#2971,.T.);
#2114=FACE_OUTER_BOUND('',#2972,.T.);
#2115=FACE_OUTER_BOUND('',#2973,.T.);
#2116=FACE_OUTER_BOUND('',#2974,.T.);
#2117=FACE_OUTER_BOUND('',#2976,.T.);
#2118=FACE_OUTER_BOUND('',#2977,.T.);
#2119=FACE_OUTER_BOUND('',#2978,.T.);
#2120=FACE_OUTER_BOUND('',#2984,.T.);
#2969=EDGE_LOOP('',(#9212,#9213,#9214,#9215));
#2970=EDGE_LOOP('',(#9216,#9217,#9218,#9219));
#2971=EDGE_LOOP('',(#9220,#9221,#9222,#9223));
#2972=EDGE_LOOP('',(#9224,#9225,#9226,#9227));
#2973=EDGE_LOOP('',(#9228,#9229,#9230,#9231));
#2974=EDGE_LOOP('',(#9232));
#2975=EDGE_LOOP('',(#9233));
#2976=EDGE_LOOP('',(#9234,#9235,#9236,#9237));
#2977=EDGE_LOOP('',(#9238,#9239,#9240,#9241));
#2978=EDGE_LOOP('',(#9242));
#2979=EDGE_LOOP('',(#9243));
#2980=EDGE_LOOP('',(#9244));
#2981=EDGE_LOOP('',(#9245));
#2982=EDGE_LOOP('',(#9246));
#2983=EDGE_LOOP('',(#9247));
#2984=EDGE_LOOP('',(#9248));
#2985=EDGE_LOOP('',(#9249));
#2986=EDGE_LOOP('',(#9250));
#2987=EDGE_LOOP('',(#9251));
#2988=EDGE_LOOP('',(#9252));
#2989=EDGE_LOOP('',(#9253));
#4204=LINE('',#21233,#4944);
#4205=LINE('',#21239,#4945);
#4206=LINE('',#21245,#4946);
#4207=LINE('',#21251,#4947);
#4208=LINE('',#21257,#4948);
#4209=LINE('',#21264,#4949);
#4210=LINE('',#21270,#4950);
#4944=VECTOR('',#16742,0.225);
#4945=VECTOR('',#16749,0.225);
#4946=VECTOR('',#16756,0.225);
#4947=VECTOR('',#16763,0.225);
#4948=VECTOR('',#16770,1.59);
#4949=VECTOR('',#16779,1.02);
#4950=VECTOR('',#16786,2.2);
#5644=CIRCLE('',#14681,0.225);
#5645=CIRCLE('',#14682,0.225);
#5646=CIRCLE('',#14684,0.225);
#5647=CIRCLE('',#14685,0.225);
#5648=CIRCLE('',#14687,0.225);
#5649=CIRCLE('',#14688,0.225);
#5650=CIRCLE('',#14690,0.225);
#5651=CIRCLE('',#14691,0.225);
#5652=CIRCLE('',#14693,1.59);
#5653=CIRCLE('',#14694,1.59);
#5654=CIRCLE('',#14696,1.02);
#5655=CIRCLE('',#14698,1.02);
#5656=CIRCLE('',#14700,2.2);
#5657=CIRCLE('',#14701,2.2);
#6463=VERTEX_POINT('',#21230);
#6464=VERTEX_POINT('',#21232);
#6465=VERTEX_POINT('',#21236);
#6466=VERTEX_POINT('',#21238);
#6467=VERTEX_POINT('',#21242);
#6468=VERTEX_POINT('',#21244);
#6469=VERTEX_POINT('',#21248);
#6470=VERTEX_POINT('',#21250);
#6471=VERTEX_POINT('',#21254);
#6472=VERTEX_POINT('',#21256);
#6473=VERTEX_POINT('',#21260);
#6474=VERTEX_POINT('',#21263);
#6475=VERTEX_POINT('',#21267);
#6476=VERTEX_POINT('',#21269);
#7541=EDGE_CURVE('',#6463,#6463,#5644,.T.);
#7542=EDGE_CURVE('',#6463,#6464,#4204,.T.);
#7543=EDGE_CURVE('',#6464,#6464,#5645,.T.);
#7544=EDGE_CURVE('',#6465,#6465,#5646,.T.);
#7545=EDGE_CURVE('',#6465,#6466,#4205,.T.);
#7546=EDGE_CURVE('',#6466,#6466,#5647,.T.);
#7547=EDGE_CURVE('',#6467,#6467,#5648,.T.);
#7548=EDGE_CURVE('',#6467,#6468,#4206,.T.);
#7549=EDGE_CURVE('',#6468,#6468,#5649,.T.);
#7550=EDGE_CURVE('',#6469,#6469,#5650,.T.);
#7551=EDGE_CURVE('',#6469,#6470,#4207,.T.);
#7552=EDGE_CURVE('',#6470,#6470,#5651,.T.);
#7553=EDGE_CURVE('',#6471,#6471,#5652,.T.);
#7554=EDGE_CURVE('',#6471,#6472,#4208,.T.);
#7555=EDGE_CURVE('',#6472,#6472,#5653,.T.);
#7556=EDGE_CURVE('',#6473,#6473,#5654,.T.);
#7557=EDGE_CURVE('',#6473,#6474,#4209,.T.);
#7558=EDGE_CURVE('',#6474,#6474,#5655,.T.);
#7559=EDGE_CURVE('',#6475,#6475,#5656,.T.);
#7560=EDGE_CURVE('',#6475,#6476,#4210,.T.);
#7561=EDGE_CURVE('',#6476,#6476,#5657,.T.);
#9212=ORIENTED_EDGE('',*,*,#7541,.F.);
#9213=ORIENTED_EDGE('',*,*,#7542,.T.);
#9214=ORIENTED_EDGE('',*,*,#7543,.F.);
#9215=ORIENTED_EDGE('',*,*,#7542,.F.);
#9216=ORIENTED_EDGE('',*,*,#7544,.F.);
#9217=ORIENTED_EDGE('',*,*,#7545,.T.);
#9218=ORIENTED_EDGE('',*,*,#7546,.F.);
#9219=ORIENTED_EDGE('',*,*,#7545,.F.);
#9220=ORIENTED_EDGE('',*,*,#7547,.F.);
#9221=ORIENTED_EDGE('',*,*,#7548,.T.);
#9222=ORIENTED_EDGE('',*,*,#7549,.F.);
#9223=ORIENTED_EDGE('',*,*,#7548,.F.);
#9224=ORIENTED_EDGE('',*,*,#7550,.F.);
#9225=ORIENTED_EDGE('',*,*,#7551,.T.);
#9226=ORIENTED_EDGE('',*,*,#7552,.F.);
#9227=ORIENTED_EDGE('',*,*,#7551,.F.);
#9228=ORIENTED_EDGE('',*,*,#7553,.F.);
#9229=ORIENTED_EDGE('',*,*,#7554,.T.);
#9230=ORIENTED_EDGE('',*,*,#7555,.F.);
#9231=ORIENTED_EDGE('',*,*,#7554,.F.);
#9232=ORIENTED_EDGE('',*,*,#7553,.T.);
#9233=ORIENTED_EDGE('',*,*,#7556,.T.);
#9234=ORIENTED_EDGE('',*,*,#7556,.F.);
#9235=ORIENTED_EDGE('',*,*,#7557,.T.);
#9236=ORIENTED_EDGE('',*,*,#7558,.T.);
#9237=ORIENTED_EDGE('',*,*,#7557,.F.);
#9238=ORIENTED_EDGE('',*,*,#7559,.F.);
#9239=ORIENTED_EDGE('',*,*,#7560,.T.);
#9240=ORIENTED_EDGE('',*,*,#7561,.T.);
#9241=ORIENTED_EDGE('',*,*,#7560,.F.);
#9242=ORIENTED_EDGE('',*,*,#7559,.T.);
#9243=ORIENTED_EDGE('',*,*,#7555,.T.);
#9244=ORIENTED_EDGE('',*,*,#7552,.T.);
#9245=ORIENTED_EDGE('',*,*,#7549,.T.);
#9246=ORIENTED_EDGE('',*,*,#7546,.T.);
#9247=ORIENTED_EDGE('',*,*,#7543,.T.);
#9248=ORIENTED_EDGE('',*,*,#7561,.F.);
#9249=ORIENTED_EDGE('',*,*,#7558,.F.);
#9250=ORIENTED_EDGE('',*,*,#7550,.T.);
#9251=ORIENTED_EDGE('',*,*,#7547,.T.);
#9252=ORIENTED_EDGE('',*,*,#7544,.T.);
#9253=ORIENTED_EDGE('',*,*,#7541,.T.);
#12094=CYLINDRICAL_SURFACE('',#14680,0.225);
#12095=CYLINDRICAL_SURFACE('',#14683,0.225);
#12096=CYLINDRICAL_SURFACE('',#14686,0.225);
#12097=CYLINDRICAL_SURFACE('',#14689,0.225);
#12098=CYLINDRICAL_SURFACE('',#14692,1.59);
#12099=CYLINDRICAL_SURFACE('',#14697,1.02);
#12100=CYLINDRICAL_SURFACE('',#14699,2.2);
#12478=ADVANCED_FACE('',(#2111),#12094,.F.);
#12479=ADVANCED_FACE('',(#2112),#12095,.F.);
#12480=ADVANCED_FACE('',(#2113),#12096,.F.);
#12481=ADVANCED_FACE('',(#2114),#12097,.F.);
#12482=ADVANCED_FACE('',(#2115),#12098,.T.);
#12483=ADVANCED_FACE('',(#2116,#1255),#1668,.T.);
#12484=ADVANCED_FACE('',(#2117),#12099,.F.);
#12485=ADVANCED_FACE('',(#2118),#12100,.T.);
#12486=ADVANCED_FACE('',(#2119,#1256,#1257,#1258,#1259,#1260),#1669,.T.);
#12487=ADVANCED_FACE('',(#2120,#1261,#1262,#1263,#1264,#1265),#1670,.F.);
#13252=CLOSED_SHELL('',(#12478,#12479,#12480,#12481,#12482,#12483,#12484,
#12485,#12486,#12487));
#14679=AXIS2_PLACEMENT_3D('',#21228,#16736,#16737);
#14680=AXIS2_PLACEMENT_3D('',#21229,#16738,#16739);
#14681=AXIS2_PLACEMENT_3D('',#21231,#16740,#16741);
#14682=AXIS2_PLACEMENT_3D('',#21234,#16743,#16744);
#14683=AXIS2_PLACEMENT_3D('',#21235,#16745,#16746);
#14684=AXIS2_PLACEMENT_3D('',#21237,#16747,#16748);
#14685=AXIS2_PLACEMENT_3D('',#21240,#16750,#16751);
#14686=AXIS2_PLACEMENT_3D('',#21241,#16752,#16753);
#14687=AXIS2_PLACEMENT_3D('',#21243,#16754,#16755);
#14688=AXIS2_PLACEMENT_3D('',#21246,#16757,#16758);
#14689=AXIS2_PLACEMENT_3D('',#21247,#16759,#16760);
#14690=AXIS2_PLACEMENT_3D('',#21249,#16761,#16762);
#14691=AXIS2_PLACEMENT_3D('',#21252,#16764,#16765);
#14692=AXIS2_PLACEMENT_3D('',#21253,#16766,#16767);
#14693=AXIS2_PLACEMENT_3D('',#21255,#16768,#16769);
#14694=AXIS2_PLACEMENT_3D('',#21258,#16771,#16772);
#14695=AXIS2_PLACEMENT_3D('',#21259,#16773,#16774);
#14696=AXIS2_PLACEMENT_3D('',#21261,#16775,#16776);
#14697=AXIS2_PLACEMENT_3D('',#21262,#16777,#16778);
#14698=AXIS2_PLACEMENT_3D('',#21265,#16780,#16781);
#14699=AXIS2_PLACEMENT_3D('',#21266,#16782,#16783);
#14700=AXIS2_PLACEMENT_3D('',#21268,#16784,#16785);
#14701=AXIS2_PLACEMENT_3D('',#21271,#16787,#16788);
#14702=AXIS2_PLACEMENT_3D('',#21272,#16789,#16790);
#14703=AXIS2_PLACEMENT_3D('',#21273,#16791,#16792);
#16736=DIRECTION('axis',(0.,0.,1.));
#16737=DIRECTION('refdir',(1.,0.,0.));
#16738=DIRECTION('center_axis',(1.,0.,0.));
#16739=DIRECTION('ref_axis',(0.,0.,-1.));
#16740=DIRECTION('center_axis',(1.,0.,0.));
#16741=DIRECTION('ref_axis',(0.,0.,-1.));
#16742=DIRECTION('',(1.,0.,0.));
#16743=DIRECTION('center_axis',(-1.,0.,0.));
#16744=DIRECTION('ref_axis',(0.,0.,-1.));
#16745=DIRECTION('center_axis',(1.,0.,0.));
#16746=DIRECTION('ref_axis',(0.,0.,-1.));
#16747=DIRECTION('center_axis',(1.,0.,0.));
#16748=DIRECTION('ref_axis',(0.,0.,-1.));
#16749=DIRECTION('',(1.,0.,0.));
#16750=DIRECTION('center_axis',(-1.,0.,0.));
#16751=DIRECTION('ref_axis',(0.,0.,-1.));
#16752=DIRECTION('center_axis',(1.,0.,0.));
#16753=DIRECTION('ref_axis',(0.,0.,-1.));
#16754=DIRECTION('center_axis',(1.,0.,0.));
#16755=DIRECTION('ref_axis',(0.,0.,-1.));
#16756=DIRECTION('',(1.,0.,0.));
#16757=DIRECTION('center_axis',(-1.,0.,0.));
#16758=DIRECTION('ref_axis',(0.,0.,-1.));
#16759=DIRECTION('center_axis',(1.,0.,0.));
#16760=DIRECTION('ref_axis',(0.,0.,-1.));
#16761=DIRECTION('center_axis',(1.,0.,0.));
#16762=DIRECTION('ref_axis',(0.,0.,-1.));
#16763=DIRECTION('',(1.,0.,0.));
#16764=DIRECTION('center_axis',(-1.,0.,0.));
#16765=DIRECTION('ref_axis',(0.,0.,-1.));
#16766=DIRECTION('center_axis',(1.,0.,0.));
#16767=DIRECTION('ref_axis',(0.,0.,-1.));
#16768=DIRECTION('center_axis',(1.,0.,0.));
#16769=DIRECTION('ref_axis',(0.,0.,-1.));
#16770=DIRECTION('',(-1.,0.,0.));
#16771=DIRECTION('center_axis',(-1.,0.,0.));
#16772=DIRECTION('ref_axis',(0.,0.,-1.));
#16773=DIRECTION('center_axis',(1.,0.,0.));
#16774=DIRECTION('ref_axis',(0.,0.,-1.));
#16775=DIRECTION('center_axis',(-1.,0.,0.));
#16776=DIRECTION('ref_axis',(0.,0.,-1.));
#16777=DIRECTION('center_axis',(1.,0.,0.));
#16778=DIRECTION('ref_axis',(0.,0.,-1.));
#16779=DIRECTION('',(-1.,0.,0.));
#16780=DIRECTION('center_axis',(-1.,0.,0.));
#16781=DIRECTION('ref_axis',(0.,0.,-1.));
#16782=DIRECTION('center_axis',(1.,0.,0.));
#16783=DIRECTION('ref_axis',(0.,0.,-1.));
#16784=DIRECTION('center_axis',(1.,0.,0.));
#16785=DIRECTION('ref_axis',(0.,0.,-1.));
#16786=DIRECTION('',(-1.,0.,0.));
#16787=DIRECTION('center_axis',(1.,0.,0.));
#16788=DIRECTION('ref_axis',(0.,0.,-1.));
#16789=DIRECTION('center_axis',(1.,0.,0.));
#16790=DIRECTION('ref_axis',(0.,0.,-1.));
#16791=DIRECTION('center_axis',(1.,0.,0.));
#16792=DIRECTION('ref_axis',(0.,0.,-1.));
#21228=CARTESIAN_POINT('',(0.,0.,0.));
#21229=CARTESIAN_POINT('Origin',(-1.4,-1.30814754519511,4.69185245480489));
#21230=CARTESIAN_POINT('',(-1.3,-1.30814754519511,4.91685245480489));
#21231=CARTESIAN_POINT('Origin',(-1.3,-1.30814754519511,4.69185245480489));
#21232=CARTESIAN_POINT('',(-1.,-1.30814754519511,4.91685245480489));
#21233=CARTESIAN_POINT('',(-1.4,-1.30814754519511,4.91685245480489));
#21234=CARTESIAN_POINT('Origin',(-1.,-1.30814754519511,4.69185245480489));
#21235=CARTESIAN_POINT('Origin',(-1.4,-1.30814754519511,7.30814754519511));
#21236=CARTESIAN_POINT('',(-1.3,-1.30814754519511,7.53314754519511));
#21237=CARTESIAN_POINT('Origin',(-1.3,-1.30814754519511,7.30814754519511));
#21238=CARTESIAN_POINT('',(-1.,-1.30814754519511,7.53314754519511));
#21239=CARTESIAN_POINT('',(-1.4,-1.30814754519511,7.53314754519511));
#21240=CARTESIAN_POINT('Origin',(-1.,-1.30814754519511,7.30814754519511));
#21241=CARTESIAN_POINT('Origin',(-1.4,1.30814754519511,7.30814754519511));
#21242=CARTESIAN_POINT('',(-1.3,1.30814754519511,7.53314754519511));
#21243=CARTESIAN_POINT('Origin',(-1.3,1.30814754519511,7.30814754519511));
#21244=CARTESIAN_POINT('',(-1.,1.30814754519511,7.53314754519511));
#21245=CARTESIAN_POINT('',(-1.4,1.30814754519511,7.53314754519511));
#21246=CARTESIAN_POINT('Origin',(-1.,1.30814754519511,7.30814754519511));
#21247=CARTESIAN_POINT('Origin',(-1.4,1.30814754519511,4.69185245480489));
#21248=CARTESIAN_POINT('',(-1.3,1.30814754519511,4.91685245480489));
#21249=CARTESIAN_POINT('Origin',(-1.3,1.30814754519511,4.69185245480489));
#21250=CARTESIAN_POINT('',(-1.,1.30814754519511,4.91685245480489));
#21251=CARTESIAN_POINT('',(-1.4,1.30814754519511,4.91685245480489));
#21252=CARTESIAN_POINT('Origin',(-1.,1.30814754519511,4.69185245480489));
#21253=CARTESIAN_POINT('Origin',(-1.,0.,6.));
#21254=CARTESIAN_POINT('',(-0.5,-1.94718841064429E-16,7.59));
#21255=CARTESIAN_POINT('Origin',(-0.5,0.,6.));
#21256=CARTESIAN_POINT('',(-1.,-1.94718841064429E-16,7.59));
#21257=CARTESIAN_POINT('',(-1.,-1.94718841064429E-16,7.59));
#21258=CARTESIAN_POINT('Origin',(-1.,0.,6.));
#21259=CARTESIAN_POINT('Origin',(-0.5,0.,6.));
#21260=CARTESIAN_POINT('',(-0.5,-1.2491397351303E-16,7.02));
#21261=CARTESIAN_POINT('Origin',(-0.5,0.,6.));
#21262=CARTESIAN_POINT('Origin',(-1.3,0.,6.));
#21263=CARTESIAN_POINT('',(-1.3,-1.2491397351303E-16,7.02));
#21264=CARTESIAN_POINT('',(-1.3,-1.2491397351303E-16,7.02));
#21265=CARTESIAN_POINT('Origin',(-1.3,0.,6.));
#21266=CARTESIAN_POINT('Origin',(-1.3,0.,6.));
#21267=CARTESIAN_POINT('',(-1.,-2.69422295812418E-16,8.2));
#21268=CARTESIAN_POINT('Origin',(-1.,0.,6.));
#21269=CARTESIAN_POINT('',(-1.3,-2.69422295812418E-16,8.2));
#21270=CARTESIAN_POINT('',(-1.3,-2.69422295812418E-16,8.2));
#21271=CARTESIAN_POINT('Origin',(-1.3,0.,6.));
#21272=CARTESIAN_POINT('Origin',(-1.,0.,6.));
#21273=CARTESIAN_POINT('Origin',(-1.3,0.,6.));
#24865=UNCERTAINTY_MEASURE_WITH_UNIT(LENGTH_MEASURE(0.001),#25101,
'DISTANCE_ACCURACY_VALUE',
'Maximum model space distance between geometric entities at asserted c
onnectivities');
#24979=UNCERTAINTY_MEASURE_WITH_UNIT(LENGTH_MEASURE(0.001),#25101,
'DISTANCE_ACCURACY_VALUE',
'Maximum model space distance between geometric entities at asserted c
onnectivities');
#24986=(
GEOMETRIC_REPRESENTATION_CONTEXT(3)
GLOBAL_UNCERTAINTY_ASSIGNED_CONTEXT((#24865))
GLOBAL_UNIT_ASSIGNED_CONTEXT((#25101,#25103,#25104))
REPRESENTATION_CONTEXT('','3D')
);
#25100=(
GEOMETRIC_REPRESENTATION_CONTEXT(3)
GLOBAL_UNCERTAINTY_ASSIGNED_CONTEXT((#24979))
GLOBAL_UNIT_ASSIGNED_CONTEXT((#25101,#25103,#25104))
REPRESENTATION_CONTEXT('','3D')
);
#25101=(
LENGTH_UNIT()
NAMED_UNIT(*)
SI_UNIT(.CENTI.,.METRE.)
);
#25103=(
NAMED_UNIT(*)
PLANE_ANGLE_UNIT()
SI_UNIT($,.RADIAN.)
);
#25104=(
NAMED_UNIT(*)
SI_UNIT($,.STERADIAN.)
SOLID_ANGLE_UNIT()
);
#25111=SHAPE_DEFINITION_REPRESENTATION(#25231,#25516);
#25231=PRODUCT_DEFINITION_SHAPE('',$,#25637);
#25516=SHAPE_REPRESENTATION('',(#14679),#24986);
#25630=PRODUCT_DEFINITION_CONTEXT('part definition',#25992,'design');
#25637=PRODUCT_DEFINITION('Screw bearing cap','Screw bearing cap',#25757,
#25630);
#25757=PRODUCT_DEFINITION_FORMATION('',$,#26000);
#25992=APPLICATION_CONTEXT(
'Core Data for Automotive Mechanical Design Process');
#25993=PRODUCT_CONTEXT('part definition',#25992,'mechanical');
#26000=PRODUCT('Screw bearing cap','Screw bearing cap',
'Screw bearing cap',(#25993));
#26192=COLOUR_RGB('Black',0.12,0.14,0.17);
#26193=FILL_AREA_STYLE_COLOUR('',#26192);
#26194=FILL_AREA_STYLE('',(#26193));
#26195=SURFACE_STYLE_FILL_AREA(#26194);
#26196=SURFACE_SIDE_STYLE('',(#26195));
#26197=SURFACE_STYLE_USAGE(.BOTH.,#26196);
#26198=PRESENTATION_STYLE_ASSIGNMENT((#26197));
ENDSEC;
END-ISO-10303-21;
